ISO-10303-21;
HEADER;
/* Generated by software containing ST-Developer
 * from STEP Tools, Inc. (www.steptools.com) 
 */

FILE_DESCRIPTION(
/* description */ (''),
/* implementation_level */ '2;1');

FILE_NAME(
/* name */ 'Shaft.step',
/* time_stamp */ '2026-10-23T22:28:14+06:00',
/* author */ (''),
/* organization */ (''),
/* preprocessor_version */ 'ST-DEVELOPER v20.2',
/* originating_system */ 'Autodesk Translation Framework v15.15.0.0',
/* authorisation */ '');

FILE_SCHEMA (('AUTOMOTIVE_DESIGN { 1 0 10303 214 3 1 1 }'));
ENDSEC;

DATA;
#10=MECHANICAL_DESIGN_GEOMETRIC_PRESENTATION_REPRESENTATION('',(#107),#6753);
#63=CONICAL_SURFACE('',#4040,5.5,0.785398163397448);
#64=CONICAL_SURFACE('',#4047,5.51285218418961,0.317172261260326);
#65=B_SPLINE_CURVE_WITH_KNOTS('',3,(#5826,#5827,#5828,#5829,#5830,#5831,
#5832,#5833),.UNSPECIFIED.,.F.,.F.,(4,2,2,4),(0.,0.191037328674406,0.382074657348811,
0.439575437008213),.UNSPECIFIED.);
#66=B_SPLINE_CURVE_WITH_KNOTS('',3,(#5837,#5838,#5839,#5840,#5841,#5842,
#5843,#5844),.UNSPECIFIED.,.F.,.F.,(4,2,2,4),(1.09233777373606,1.14983855339546,
1.34087588206987,1.53191321074428),.UNSPECIFIED.);
#67=B_SPLINE_CURVE_WITH_KNOTS('',3,(#5845,#5846,#5847,#5848,#5849,#5850,
#5851,#5852),.UNSPECIFIED.,.F.,.F.,(4,2,2,4),(1.53191321074428,1.72295053941868,
1.91398786809309,1.97148864775249),.UNSPECIFIED.);
#68=B_SPLINE_CURVE_WITH_KNOTS('',3,(#5853,#5854,#5855,#5856,#5857,#5858,
#5859,#5860),.UNSPECIFIED.,.F.,.F.,(4,2,2,4),(-0.439575436976826,-0.382074657348811,
-0.191037328674406,0.),.UNSPECIFIED.);
#70=(
BOUNDED_CURVE()
B_SPLINE_CURVE(2,(#5813,#5814,#5815),.UNSPECIFIED.,.F.,.F.)
B_SPLINE_CURVE_WITH_KNOTS((3,3),(0.0138131398228909,0.0359194684117599),
 .UNSPECIFIED.)
CURVE()
GEOMETRIC_REPRESENTATION_ITEM()
RATIONAL_B_SPLINE_CURVE((1.00006551876347,1.00008518697359,1.))
REPRESENTATION_ITEM('')
);
#71=(
BOUNDED_CURVE()
B_SPLINE_CURVE(2,(#5819,#5820,#5821),.UNSPECIFIED.,.F.,.F.)
B_SPLINE_CURVE_WITH_KNOTS((3,3),(0.,0.022106328588869),.UNSPECIFIED.)
CURVE()
GEOMETRIC_REPRESENTATION_ITEM()
RATIONAL_B_SPLINE_CURVE((1.,1.00008518697359,1.00006551876347))
REPRESENTATION_ITEM('')
);
#72=(
BOUNDED_CURVE()
B_SPLINE_CURVE(2,(#5863,#5864,#5865),.UNSPECIFIED.,.F.,.F.)
B_SPLINE_CURVE_WITH_KNOTS((3,3),(0.,0.022106328588869),.UNSPECIFIED.)
CURVE()
GEOMETRIC_REPRESENTATION_ITEM()
RATIONAL_B_SPLINE_CURVE((1.,1.00008518697359,1.00006551876347))
REPRESENTATION_ITEM('')
);
#73=(
BOUNDED_CURVE()
B_SPLINE_CURVE(2,(#5868,#5869,#5870),.UNSPECIFIED.,.F.,.F.)
B_SPLINE_CURVE_WITH_KNOTS((3,3),(0.0138131398228909,0.0359194684117599),
 .UNSPECIFIED.)
CURVE()
GEOMETRIC_REPRESENTATION_ITEM()
RATIONAL_B_SPLINE_CURVE((1.00006551876347,1.00008518697359,1.))
REPRESENTATION_ITEM('')
);
#75=SPHERICAL_SURFACE('',#4036,40.);
#76=SPHERICAL_SURFACE('',#4038,40.);
#81=SHAPE_REPRESENTATION_RELATIONSHIP('SRR','None',#6804,#94);
#94=ADVANCED_BREP_SHAPE_REPRESENTATION('',(#120),#6744);
#107=STYLED_ITEM('',(#6921),#120);
#120=MANIFOLD_SOLID_BREP('Shaft',#3756);
#206=PLANE('',#4029);
#207=PLANE('',#4034);
#208=PLANE('',#4046);
#382=FACE_OUTER_BOUND('',#636,.T.);
#383=FACE_OUTER_BOUND('',#637,.T.);
#384=FACE_OUTER_BOUND('',#638,.T.);
#385=FACE_OUTER_BOUND('',#639,.T.);
#386=FACE_OUTER_BOUND('',#640,.T.);
#387=FACE_OUTER_BOUND('',#641,.T.);
#388=FACE_OUTER_BOUND('',#642,.T.);
#389=FACE_OUTER_BOUND('',#643,.T.);
#390=FACE_OUTER_BOUND('',#644,.T.);
#636=EDGE_LOOP('',(#2686,#2687,#2688,#2689));
#637=EDGE_LOOP('',(#2690,#2691,#2692,#2693,#2694,#2695));
#638=EDGE_LOOP('',(#2696,#2697,#2698,#2699));
#639=EDGE_LOOP('',(#2700,#2701));
#640=EDGE_LOOP('',(#2702,#2703));
#641=EDGE_LOOP('',(#2704,#2705,#2706,#2707,#2708));
#642=EDGE_LOOP('',(#2709,#2710,#2711,#2712,#2713));
#643=EDGE_LOOP('',(#2714));
#644=EDGE_LOOP('',(#2715,#2716,#2717,#2718,#2719,#2720,#2721,#2722,#2723,
#2724,#2725,#2726,#2727));
#881=CIRCLE('',#4030,40.);
#882=CIRCLE('',#4031,39.7994974842648);
#883=CIRCLE('',#4033,40.);
#884=CIRCLE('',#4035,39.7994974842648);
#885=CIRCLE('',#4037,5.02570436837922);
#886=CIRCLE('',#4039,5.02570436837922);
#887=CIRCLE('',#4041,5.);
#888=CIRCLE('',#4042,6.);
#889=CIRCLE('',#4043,6.);
#890=CIRCLE('',#4045,6.);
#1082=LINE('',#5879,#1368);
#1083=LINE('',#5885,#1369);
#1084=LINE('',#5889,#1370);
#1368=VECTOR('',#4681,5.5);
#1369=VECTOR('',#4688,6.);
#1370=VECTOR('',#4695,5.51285218418961);
#1681=VERTEX_POINT('',#5811);
#1682=VERTEX_POINT('',#5812);
#1683=VERTEX_POINT('',#5816);
#1684=VERTEX_POINT('',#5818);
#1685=VERTEX_POINT('',#5824);
#1686=VERTEX_POINT('',#5825);
#1687=VERTEX_POINT('',#5834);
#1688=VERTEX_POINT('',#5836);
#1689=VERTEX_POINT('',#5862);
#1690=VERTEX_POINT('',#5866);
#1691=VERTEX_POINT('',#5876);
#1692=VERTEX_POINT('',#5878);
#1693=VERTEX_POINT('',#5880);
#1694=VERTEX_POINT('',#5884);
#2060=EDGE_CURVE('',#1681,#1682,#70,.T.);
#2061=EDGE_CURVE('',#1683,#1681,#881,.T.);
#2062=EDGE_CURVE('',#1684,#1683,#71,.T.);
#2063=EDGE_CURVE('',#1682,#1684,#882,.T.);
#2064=EDGE_CURVE('',#1685,#1686,#65,.T.);
#2065=EDGE_CURVE('',#1686,#1687,#883,.T.);
#2066=EDGE_CURVE('',#1687,#1688,#66,.T.);
#2067=EDGE_CURVE('',#1688,#1683,#67,.T.);
#2068=EDGE_CURVE('',#1681,#1685,#68,.T.);
#2069=EDGE_CURVE('',#1689,#1686,#72,.T.);
#2070=EDGE_CURVE('',#1690,#1689,#884,.T.);
#2071=EDGE_CURVE('',#1687,#1690,#73,.T.);
#2072=EDGE_CURVE('',#1690,#1689,#885,.T.);
#2073=EDGE_CURVE('',#1682,#1684,#886,.T.);
#2074=EDGE_CURVE('',#1691,#1691,#887,.T.);
#2075=EDGE_CURVE('',#1691,#1692,#1082,.T.);
#2076=EDGE_CURVE('',#1692,#1693,#888,.T.);
#2077=EDGE_CURVE('',#1693,#1692,#889,.T.);
#2078=EDGE_CURVE('',#1693,#1694,#1083,.T.);
#2079=EDGE_CURVE('',#1694,#1694,#890,.T.);
#2080=EDGE_CURVE('',#1694,#1685,#1084,.T.);
#2686=ORIENTED_EDGE('',*,*,#2060,.F.);
#2687=ORIENTED_EDGE('',*,*,#2061,.F.);
#2688=ORIENTED_EDGE('',*,*,#2062,.F.);
#2689=ORIENTED_EDGE('',*,*,#2063,.F.);
#2690=ORIENTED_EDGE('',*,*,#2064,.T.);
#2691=ORIENTED_EDGE('',*,*,#2065,.T.);
#2692=ORIENTED_EDGE('',*,*,#2066,.T.);
#2693=ORIENTED_EDGE('',*,*,#2067,.T.);
#2694=ORIENTED_EDGE('',*,*,#2061,.T.);
#2695=ORIENTED_EDGE('',*,*,#2068,.T.);
#2696=ORIENTED_EDGE('',*,*,#2069,.F.);
#2697=ORIENTED_EDGE('',*,*,#2070,.F.);
#2698=ORIENTED_EDGE('',*,*,#2071,.F.);
#2699=ORIENTED_EDGE('',*,*,#2065,.F.);
#2700=ORIENTED_EDGE('',*,*,#2070,.T.);
#2701=ORIENTED_EDGE('',*,*,#2072,.F.);
#2702=ORIENTED_EDGE('',*,*,#2063,.T.);
#2703=ORIENTED_EDGE('',*,*,#2073,.F.);
#2704=ORIENTED_EDGE('',*,*,#2074,.T.);
#2705=ORIENTED_EDGE('',*,*,#2075,.T.);
#2706=ORIENTED_EDGE('',*,*,#2076,.T.);
#2707=ORIENTED_EDGE('',*,*,#2077,.T.);
#2708=ORIENTED_EDGE('',*,*,#2075,.F.);
#2709=ORIENTED_EDGE('',*,*,#2076,.F.);
#2710=ORIENTED_EDGE('',*,*,#2077,.F.);
#2711=ORIENTED_EDGE('',*,*,#2078,.T.);
#2712=ORIENTED_EDGE('',*,*,#2079,.T.);
#2713=ORIENTED_EDGE('',*,*,#2078,.F.);
#2714=ORIENTED_EDGE('',*,*,#2074,.F.);
#2715=ORIENTED_EDGE('',*,*,#2079,.F.);
#2716=ORIENTED_EDGE('',*,*,#2080,.T.);
#2717=ORIENTED_EDGE('',*,*,#2068,.F.);
#2718=ORIENTED_EDGE('',*,*,#2060,.T.);
#2719=ORIENTED_EDGE('',*,*,#2073,.T.);
#2720=ORIENTED_EDGE('',*,*,#2062,.T.);
#2721=ORIENTED_EDGE('',*,*,#2067,.F.);
#2722=ORIENTED_EDGE('',*,*,#2066,.F.);
#2723=ORIENTED_EDGE('',*,*,#2071,.T.);
#2724=ORIENTED_EDGE('',*,*,#2072,.T.);
#2725=ORIENTED_EDGE('',*,*,#2069,.T.);
#2726=ORIENTED_EDGE('',*,*,#2064,.F.);
#2727=ORIENTED_EDGE('',*,*,#2080,.F.);
#3506=CYLINDRICAL_SURFACE('',#4032,40.);
#3507=CYLINDRICAL_SURFACE('',#4044,6.);
#3588=ADVANCED_FACE('',(#382),#206,.T.);
#3589=ADVANCED_FACE('',(#383),#3506,.F.);
#3590=ADVANCED_FACE('',(#384),#207,.F.);
#3591=ADVANCED_FACE('',(#385),#75,.F.);
#3592=ADVANCED_FACE('',(#386),#76,.F.);
#3593=ADVANCED_FACE('',(#387),#63,.T.);
#3594=ADVANCED_FACE('',(#388),#3507,.T.);
#3595=ADVANCED_FACE('',(#389),#208,.T.);
#3596=ADVANCED_FACE('',(#390),#64,.T.);
#3756=CLOSED_SHELL('',(#3588,#3589,#3590,#3591,#3592,#3593,#3594,#3595,
#3596));
#4028=AXIS2_PLACEMENT_3D('',#5809,#4653,#4654);
#4029=AXIS2_PLACEMENT_3D('',#5810,#4655,#4656);
#4030=AXIS2_PLACEMENT_3D('',#5817,#4657,#4658);
#4031=AXIS2_PLACEMENT_3D('',#5822,#4659,#4660);
#4032=AXIS2_PLACEMENT_3D('',#5823,#4661,#4662);
#4033=AXIS2_PLACEMENT_3D('',#5835,#4663,#4664);
#4034=AXIS2_PLACEMENT_3D('',#5861,#4665,#4666);
#4035=AXIS2_PLACEMENT_3D('',#5867,#4667,#4668);
#4036=AXIS2_PLACEMENT_3D('',#5871,#4669,#4670);
#4037=AXIS2_PLACEMENT_3D('',#5872,#4671,#4672);
#4038=AXIS2_PLACEMENT_3D('',#5873,#4673,#4674);
#4039=AXIS2_PLACEMENT_3D('',#5874,#4675,#4676);
#4040=AXIS2_PLACEMENT_3D('',#5875,#4677,#4678);
#4041=AXIS2_PLACEMENT_3D('',#5877,#4679,#4680);
#4042=AXIS2_PLACEMENT_3D('',#5881,#4682,#4683);
#4043=AXIS2_PLACEMENT_3D('',#5882,#4684,#4685);
#4044=AXIS2_PLACEMENT_3D('',#5883,#4686,#4687);
#4045=AXIS2_PLACEMENT_3D('',#5886,#4689,#4690);
#4046=AXIS2_PLACEMENT_3D('',#5887,#4691,#4692);
#4047=AXIS2_PLACEMENT_3D('',#5888,#4693,#4694);
#4653=DIRECTION('axis',(0.,0.,1.));
#4654=DIRECTION('refdir',(1.,0.,0.));
#4655=DIRECTION('center_axis',(0.,1.,0.));
#4656=DIRECTION('ref_axis',(1.,0.,0.));
#4657=DIRECTION('center_axis',(0.,-1.,0.));
#4658=DIRECTION('ref_axis',(1.,0.,0.));
#4659=DIRECTION('center_axis',(0.,1.,0.));
#4660=DIRECTION('ref_axis',(0.,0.,1.));
#4661=DIRECTION('center_axis',(0.,1.,0.));
#4662=DIRECTION('ref_axis',(1.,0.,0.));
#4663=DIRECTION('center_axis',(0.,1.,0.));
#4664=DIRECTION('ref_axis',(1.,0.,0.));
#4665=DIRECTION('center_axis',(0.,1.,0.));
#4666=DIRECTION('ref_axis',(1.,0.,0.));
#4667=DIRECTION('center_axis',(0.,-1.,0.));
#4668=DIRECTION('ref_axis',(0.,0.,-1.));
#4669=DIRECTION('center_axis',(6.12323399573677E-17,0.,1.));
#4670=DIRECTION('ref_axis',(1.,0.,0.));
#4671=DIRECTION('center_axis',(0.,0.,-1.));
#4672=DIRECTION('ref_axis',(1.,0.,0.));
#4673=DIRECTION('center_axis',(6.12323399573677E-17,0.,1.));
#4674=DIRECTION('ref_axis',(1.,0.,0.));
#4675=DIRECTION('center_axis',(0.,0.,-1.));
#4676=DIRECTION('ref_axis',(1.,0.,0.));
#4677=DIRECTION('center_axis',(0.,0.,1.));
#4678=DIRECTION('ref_axis',(1.,0.,0.));
#4679=DIRECTION('center_axis',(0.,0.,1.));
#4680=DIRECTION('ref_axis',(1.,0.,0.));
#4681=DIRECTION('',(-0.707106781186547,8.65956056235493E-17,0.707106781186548));
#4682=DIRECTION('center_axis',(0.,0.,-1.));
#4683=DIRECTION('ref_axis',(1.,0.,0.));
#4684=DIRECTION('center_axis',(0.,0.,-1.));
#4685=DIRECTION('ref_axis',(1.,0.,0.));
#4686=DIRECTION('center_axis',(0.,0.,-1.));
#4687=DIRECTION('ref_axis',(-1.,0.,0.));
#4688=DIRECTION('',(0.,0.,1.));
#4689=DIRECTION('center_axis',(0.,0.,-1.));
#4690=DIRECTION('ref_axis',(1.,0.,0.));
#4691=DIRECTION('center_axis',(0.,0.,-1.));
#4692=DIRECTION('ref_axis',(-1.,0.,0.));
#4693=DIRECTION('center_axis',(0.,0.,-1.));
#4694=DIRECTION('ref_axis',(-1.,0.,0.));
#4695=DIRECTION('',(-0.311881116775508,3.81944211373628E-17,0.9501211338555));
#5809=CARTESIAN_POINT('',(0.,0.,0.));
#5810=CARTESIAN_POINT('Origin',(0.,-4.,114.33240815703));
#5811=CARTESIAN_POINT('',(3.14621650000503,-4.,74.4563336042978));
#5812=CARTESIAN_POINT('',(3.04264759680545,-4.,74.6493853941201));
#5813=CARTESIAN_POINT('Ctrl Pts',(3.14621650000503,-4.,74.4563336042978));
#5814=CARTESIAN_POINT('Ctrl Pts',(3.09410761398192,-4.,74.5544748329615));
#5815=CARTESIAN_POINT('Ctrl Pts',(3.04264759680544,-4.,74.6493853941201));
#5816=CARTESIAN_POINT('',(-3.14621650000503,-4.,74.4563336042978));
#5817=CARTESIAN_POINT('Origin',(0.,-4.,114.33240815703));
#5818=CARTESIAN_POINT('',(-3.04264759680545,-4.,74.6493853941201));
#5819=CARTESIAN_POINT('Ctrl Pts',(-3.04264759680544,-4.,74.6493853941201));
#5820=CARTESIAN_POINT('Ctrl Pts',(-3.09410761398192,-4.,74.5544748329615));
#5821=CARTESIAN_POINT('Ctrl Pts',(-3.14621650000503,-4.,74.4563336042978));
#5822=CARTESIAN_POINT('Origin',(-4.44089209850063E-15,-4.,114.33240815703));
#5823=CARTESIAN_POINT('Origin',(0.,0.,114.33240815703));
#5824=CARTESIAN_POINT('',(5.02570436837922,0.,74.6493853941201));
#5825=CARTESIAN_POINT('',(3.14621650000503,4.,74.4563336042978));
#5826=CARTESIAN_POINT('Ctrl Pts',(5.0257043683792,1.38777878078145E-16,
74.6493853941202));
#5827=CARTESIAN_POINT('Ctrl Pts',(5.0257043683792,0.636791095581352,74.6493853941202));
#5828=CARTESIAN_POINT('Ctrl Pts',(4.90246224678715,1.31704352377502,74.63316071429));
#5829=CARTESIAN_POINT('Ctrl Pts',(4.39842345787458,2.57251995336055,74.5741605152364));
#5830=CARTESIAN_POINT('Ctrl Pts',(4.01759790991964,3.14777098226807,74.5322097357543));
#5831=CARTESIAN_POINT('Ctrl Pts',(3.44263279831291,3.74199212690276,74.4806062316187));
#5832=CARTESIAN_POINT('Ctrl Pts',(3.29909000169272,3.87471942228721,74.4683953014136));
#5833=CARTESIAN_POINT('Ctrl Pts',(3.14621650000503,4.,74.4563336042978));
#5834=CARTESIAN_POINT('',(-3.14621650000503,4.,74.4563336042978));
#5835=CARTESIAN_POINT('Origin',(0.,4.,114.33240815703));
#5836=CARTESIAN_POINT('',(-5.02570436837922,0.,74.6493853941201));
#5837=CARTESIAN_POINT('Ctrl Pts',(-3.14621650000503,4.,74.4563336042978));
#5838=CARTESIAN_POINT('Ctrl Pts',(-3.29909000169272,3.87471942228721,74.4683953014136));
#5839=CARTESIAN_POINT('Ctrl Pts',(-3.4426327983129,3.74199212690276,74.4806062316187));
#5840=CARTESIAN_POINT('Ctrl Pts',(-4.01759790991964,3.14777098226807,74.5322097357543));
#5841=CARTESIAN_POINT('Ctrl Pts',(-4.39842345787458,2.57251995336055,74.5741605152364));
#5842=CARTESIAN_POINT('Ctrl Pts',(-4.90246224678715,1.31704352377502,74.63316071429));
#5843=CARTESIAN_POINT('Ctrl Pts',(-5.0257043683792,0.636791095581352,74.6493853941202));
#5844=CARTESIAN_POINT('Ctrl Pts',(-5.0257043683792,0.,74.6493853941202));
#5845=CARTESIAN_POINT('Ctrl Pts',(-5.0257043683792,4.16333634234434E-16,
74.6493853941202));
#5846=CARTESIAN_POINT('Ctrl Pts',(-5.0257043683792,-0.636791095581351,74.6493853941202));
#5847=CARTESIAN_POINT('Ctrl Pts',(-4.90246224678715,-1.31704352377502,74.63316071429));
#5848=CARTESIAN_POINT('Ctrl Pts',(-4.39842345787458,-2.57251995336055,74.5741605152364));
#5849=CARTESIAN_POINT('Ctrl Pts',(-4.01759790991964,-3.14777098226807,74.5322097357543));
#5850=CARTESIAN_POINT('Ctrl Pts',(-3.44263279831291,-3.74199212690276,74.4806062316187));
#5851=CARTESIAN_POINT('Ctrl Pts',(-3.29909000169272,-3.87471942228721,74.4683953014136));
#5852=CARTESIAN_POINT('Ctrl Pts',(-3.14621650000503,-4.,74.4563336042978));
#5853=CARTESIAN_POINT('Ctrl Pts',(3.14621650000503,-4.,74.4563336042978));
#5854=CARTESIAN_POINT('Ctrl Pts',(3.29909000173959,-3.8747194222488,74.4683953014173));
#5855=CARTESIAN_POINT('Ctrl Pts',(3.44263279838552,-3.74199212682772,74.4806062316253));
#5856=CARTESIAN_POINT('Ctrl Pts',(4.01759790991964,-3.14777098226807,74.5322097357543));
#5857=CARTESIAN_POINT('Ctrl Pts',(4.39842345787458,-2.57251995336055,74.5741605152364));
#5858=CARTESIAN_POINT('Ctrl Pts',(4.90246224678715,-1.31704352377502,74.63316071429));
#5859=CARTESIAN_POINT('Ctrl Pts',(5.0257043683792,-0.636791095581352,74.6493853941202));
#5860=CARTESIAN_POINT('Ctrl Pts',(5.0257043683792,-4.16333634234434E-16,
74.6493853941202));
#5861=CARTESIAN_POINT('Origin',(0.,4.,114.33240815703));
#5862=CARTESIAN_POINT('',(3.04264759680545,4.,74.6493853941201));
#5863=CARTESIAN_POINT('Ctrl Pts',(3.04264759680544,4.,74.6493853941201));
#5864=CARTESIAN_POINT('Ctrl Pts',(3.09410761398192,4.,74.5544748329615));
#5865=CARTESIAN_POINT('Ctrl Pts',(3.14621650000503,4.,74.4563336042978));
#5866=CARTESIAN_POINT('',(-3.04264759680545,4.,74.6493853941201));
#5867=CARTESIAN_POINT('Origin',(-4.44089209850063E-15,4.,114.33240815703));
#5868=CARTESIAN_POINT('Ctrl Pts',(-3.14621650000503,4.,74.4563336042978));
#5869=CARTESIAN_POINT('Ctrl Pts',(-3.09410761398192,4.,74.5544748329615));
#5870=CARTESIAN_POINT('Ctrl Pts',(-3.04264759680544,4.,74.6493853941201));
#5871=CARTESIAN_POINT('Origin',(-4.44089209850063E-15,0.,114.33240815703));
#5872=CARTESIAN_POINT('Origin',(0.,0.,74.6493853941201));
#5873=CARTESIAN_POINT('Origin',(-4.44089209850063E-15,0.,114.33240815703));
#5874=CARTESIAN_POINT('Origin',(0.,0.,74.6493853941201));
#5875=CARTESIAN_POINT('Origin',(0.,0.,0.5));
#5876=CARTESIAN_POINT('',(-5.,-6.12323399573677E-16,0.));
#5877=CARTESIAN_POINT('Origin',(0.,0.,0.));
#5878=CARTESIAN_POINT('',(-6.,7.34788079488412E-16,1.));
#5879=CARTESIAN_POINT('',(-5.5,6.73555739531044E-16,0.5));
#5880=CARTESIAN_POINT('',(6.,-7.34788079488412E-16,1.));
#5881=CARTESIAN_POINT('Origin',(0.,0.,1.));
#5882=CARTESIAN_POINT('Origin',(0.,0.,1.));
#5883=CARTESIAN_POINT('Origin',(0.,0.,35.8406354386459));
#5884=CARTESIAN_POINT('',(6.,-7.34788079488412E-16,71.6812708772919));
#5885=CARTESIAN_POINT('',(6.,-7.34788079488412E-16,35.8406354386459));
#5886=CARTESIAN_POINT('Origin',(0.,0.,71.6812708772919));
#5887=CARTESIAN_POINT('Origin',(0.,0.,0.));
#5888=CARTESIAN_POINT('Origin',(0.,0.,73.165328135706));
#5889=CARTESIAN_POINT('',(5.51285218418961,-6.7512967815403E-16,73.165328135706));
#6729=UNCERTAINTY_MEASURE_WITH_UNIT(LENGTH_MEASURE(0.01),#6754,
'DISTANCE_ACCURACY_VALUE',
'Maximum model space distance between geometric entities at asserted c
onnectivities');
#6738=UNCERTAINTY_MEASURE_WITH_UNIT(LENGTH_MEASURE(0.01),#6754,
'DISTANCE_ACCURACY_VALUE',
'Maximum model space distance between geometric entities at asserted c
onnectivities');
#6744=(
GEOMETRIC_REPRESENTATION_CONTEXT(3)
GLOBAL_UNCERTAINTY_ASSIGNED_CONTEXT((#6729))
GLOBAL_UNIT_ASSIGNED_CONTEXT((#6754,#6756,#6757))
REPRESENTATION_CONTEXT('','3D')
);
#6753=(
GEOMETRIC_REPRESENTATION_CONTEXT(3)
GLOBAL_UNCERTAINTY_ASSIGNED_CONTEXT((#6738))
GLOBAL_UNIT_ASSIGNED_CONTEXT((#6754,#6756,#6757))
REPRESENTATION_CONTEXT('','3D')
);
#6754=(
LENGTH_UNIT()
NAMED_UNIT(*)
SI_UNIT(.MILLI.,.METRE.)
);
#6756=(
NAMED_UNIT(*)
PLANE_ANGLE_UNIT()
SI_UNIT($,.RADIAN.)
);
#6757=(
NAMED_UNIT(*)
SI_UNIT($,.STERADIAN.)
SOLID_ANGLE_UNIT()
);
#6763=SHAPE_DEFINITION_REPRESENTATION(#6777,#6804);
#6777=PRODUCT_DEFINITION_SHAPE('',$,#6819);
#6804=SHAPE_REPRESENTATION('',(#4028),#6744);
#6813=PRODUCT_DEFINITION_CONTEXT('part definition',#6857,'design');
#6819=PRODUCT_DEFINITION('Shaft','Shaft',#6833,#6813);
#6833=PRODUCT_DEFINITION_FORMATION('',$,#6864);
#6857=APPLICATION_CONTEXT(
'Core Data for Automotive Mechanical Design Process');
#6858=PRODUCT_CONTEXT('part definition',#6857,'mechanical');
#6864=PRODUCT('Shaft','Shaft',$,(#6858));
#6915=COLOUR_RGB('Grey',0.48,0.52,0.57);
#6916=FILL_AREA_STYLE_COLOUR('',#6915);
#6917=FILL_AREA_STYLE('',(#6916));
#6918=SURFACE_STYLE_FILL_AREA(#6917);
#6919=SURFACE_SIDE_STYLE('',(#6918));
#6920=SURFACE_STYLE_USAGE(.BOTH.,#6919);
#6921=PRESENTATION_STYLE_ASSIGNMENT((#6920));
ENDSEC;
END-ISO-10303-21;
